ISO-10303-21;
HEADER;
/* Generated by software containing ST-Developer
 * from STEP Tools, Inc. (www.steptools.com) 
 */

FILE_DESCRIPTION(
/* description */ ('Drill jig with bushing plate'),
/* implementation_level */ '2;1');

FILE_NAME(
/* name */ 'M4x10 Cap Screw.step',
/* time_stamp */ '2026-10-27T10:51:08-07:00',
/* author */ (''),
/* organization */ (''),
/* preprocessor_version */ 'ST-DEVELOPER v20.2',
/* originating_system */ 'Autodesk Translation Framework v15.17.0.0',
/* authorisation */ '');

FILE_SCHEMA (('AUTOMOTIVE_DESIGN { 1 0 10303 214 3 1 1 }'));
ENDSEC;

DATA;
#10=MECHANICAL_DESIGN_GEOMETRIC_PRESENTATION_REPRESENTATION('',(#239),#6638);
#166=CONICAL_SURFACE('',#4168,0.325,0.785398163397448);
#167=CONICAL_SURFACE('',#4172,0.335,0.785398163397448);
#168=CONICAL_SURFACE('',#4176,0.21,0.463647609000806);
#170=ORIENTED_CLOSED_SHELL('',*,#3607,.F.);
#172=BREP_WITH_VOIDS('Body1',#3608,(#170));
#191=SHAPE_REPRESENTATION_RELATIONSHIP('SRR','None',#6755,#215);
#215=ADVANCED_BREP_SHAPE_REPRESENTATION('',(#172),#6628);
#239=STYLED_ITEM('',(#6950),#172);
#344=FACE_BOUND('',#943,.T.);
#453=PLANE('',#4156);
#454=PLANE('',#4157);
#455=PLANE('',#4158);
#456=PLANE('',#4159);
#457=PLANE('',#4160);
#458=PLANE('',#4161);
#459=PLANE('',#4162);
#460=PLANE('',#4163);
#461=PLANE('',#4164);
#462=PLANE('',#4166);
#463=PLANE('',#4174);
#640=FACE_OUTER_BOUND('',#929,.T.);
#641=FACE_OUTER_BOUND('',#930,.T.);
#642=FACE_OUTER_BOUND('',#931,.T.);
#643=FACE_OUTER_BOUND('',#932,.T.);
#644=FACE_OUTER_BOUND('',#933,.T.);
#645=FACE_OUTER_BOUND('',#934,.T.);
#646=FACE_OUTER_BOUND('',#935,.T.);
#647=FACE_OUTER_BOUND('',#936,.T.);
#648=FACE_OUTER_BOUND('',#937,.T.);
#649=FACE_OUTER_BOUND('',#938,.T.);
#650=FACE_OUTER_BOUND('',#939,.T.);
#651=FACE_OUTER_BOUND('',#940,.T.);
#652=FACE_OUTER_BOUND('',#941,.T.);
#653=FACE_OUTER_BOUND('',#942,.T.);
#654=FACE_OUTER_BOUND('',#944,.T.);
#655=FACE_OUTER_BOUND('',#945,.T.);
#929=EDGE_LOOP('',(#2999,#3000,#3001,#3002));
#930=EDGE_LOOP('',(#3003,#3004,#3005,#3006));
#931=EDGE_LOOP('',(#3007,#3008,#3009,#3010));
#932=EDGE_LOOP('',(#3011,#3012,#3013,#3014));
#933=EDGE_LOOP('',(#3015,#3016,#3017,#3018));
#934=EDGE_LOOP('',(#3019,#3020,#3021,#3022));
#935=EDGE_LOOP('',(#3023,#3024,#3025,#3026,#3027,#3028));
#936=EDGE_LOOP('',(#3029,#3030,#3031,#3032,#3033,#3034));
#937=EDGE_LOOP('',(#3035));
#938=EDGE_LOOP('',(#3036));
#939=EDGE_LOOP('',(#3037,#3038,#3039,#3040));
#940=EDGE_LOOP('',(#3041,#3042,#3043,#3044));
#941=EDGE_LOOP('',(#3045,#3046,#3047,#3048));
#942=EDGE_LOOP('',(#3049));
#943=EDGE_LOOP('',(#3050));
#944=EDGE_LOOP('',(#3051,#3052,#3053,#3054));
#945=EDGE_LOOP('',(#3055,#3056,#3057,#3058));
#1192=LINE('',#6213,#1453);
#1193=LINE('',#6215,#1454);
#1194=LINE('',#6217,#1455);
#1195=LINE('',#6218,#1456);
#1196=LINE('',#6221,#1457);
#1197=LINE('',#6223,#1458);
#1198=LINE('',#6224,#1459);
#1199=LINE('',#6227,#1460);
#1200=LINE('',#6229,#1461);
#1201=LINE('',#6230,#1462);
#1202=LINE('',#6233,#1463);
#1203=LINE('',#6235,#1464);
#1204=LINE('',#6236,#1465);
#1205=LINE('',#6239,#1466);
#1206=LINE('',#6241,#1467);
#1207=LINE('',#6242,#1468);
#1208=LINE('',#6244,#1469);
#1209=LINE('',#6245,#1470);
#1210=LINE('',#6257,#1471);
#1211=LINE('',#6261,#1472);
#1212=LINE('',#6265,#1473);
#1213=LINE('',#6272,#1474);
#1214=LINE('',#6274,#1475);
#1453=VECTOR('',#5043,1.);
#1454=VECTOR('',#5044,1.);
#1455=VECTOR('',#5045,1.);
#1456=VECTOR('',#5046,1.);
#1457=VECTOR('',#5049,1.);
#1458=VECTOR('',#5050,1.);
#1459=VECTOR('',#5051,1.);
#1460=VECTOR('',#5054,1.);
#1461=VECTOR('',#5055,1.);
#1462=VECTOR('',#5056,1.);
#1463=VECTOR('',#5059,1.);
#1464=VECTOR('',#5060,1.);
#1465=VECTOR('',#5061,1.);
#1466=VECTOR('',#5064,1.);
#1467=VECTOR('',#5065,1.);
#1468=VECTOR('',#5066,1.);
#1469=VECTOR('',#5069,1.);
#1470=VECTOR('',#5070,1.);
#1471=VECTOR('',#5087,0.325);
#1472=VECTOR('',#5092,0.35);
#1473=VECTOR('',#5097,0.335);
#1474=VECTOR('',#5106,0.21);
#1475=VECTOR('',#5109,0.2);
#1669=CIRCLE('',#4165,0.1954);
#1670=CIRCLE('',#4167,0.3);
#1671=CIRCLE('',#4169,0.35);
#1672=CIRCLE('',#4171,0.35);
#1673=CIRCLE('',#4173,0.32);
#1674=CIRCLE('',#4175,0.22);
#1675=CIRCLE('',#4177,0.1954);
#1907=VERTEX_POINT('',#6211);
#1908=VERTEX_POINT('',#6212);
#1909=VERTEX_POINT('',#6214);
#1910=VERTEX_POINT('',#6216);
#1911=VERTEX_POINT('',#6220);
#1912=VERTEX_POINT('',#6222);
#1913=VERTEX_POINT('',#6226);
#1914=VERTEX_POINT('',#6228);
#1915=VERTEX_POINT('',#6232);
#1916=VERTEX_POINT('',#6234);
#1917=VERTEX_POINT('',#6238);
#1918=VERTEX_POINT('',#6240);
#1919=VERTEX_POINT('',#6249);
#1920=VERTEX_POINT('',#6252);
#1921=VERTEX_POINT('',#6255);
#1922=VERTEX_POINT('',#6259);
#1923=VERTEX_POINT('',#6263);
#1924=VERTEX_POINT('',#6267);
#1925=VERTEX_POINT('',#6270);
#2287=EDGE_CURVE('',#1907,#1908,#1192,.T.);
#2288=EDGE_CURVE('',#1908,#1909,#1193,.T.);
#2289=EDGE_CURVE('',#1909,#1910,#1194,.T.);
#2290=EDGE_CURVE('',#1907,#1910,#1195,.T.);
#2291=EDGE_CURVE('',#1908,#1911,#1196,.T.);
#2292=EDGE_CURVE('',#1911,#1912,#1197,.T.);
#2293=EDGE_CURVE('',#1912,#1909,#1198,.T.);
#2294=EDGE_CURVE('',#1911,#1913,#1199,.T.);
#2295=EDGE_CURVE('',#1913,#1914,#1200,.T.);
#2296=EDGE_CURVE('',#1914,#1912,#1201,.T.);
#2297=EDGE_CURVE('',#1913,#1915,#1202,.T.);
#2298=EDGE_CURVE('',#1915,#1916,#1203,.T.);
#2299=EDGE_CURVE('',#1916,#1914,#1204,.T.);
#2300=EDGE_CURVE('',#1915,#1917,#1205,.T.);
#2301=EDGE_CURVE('',#1917,#1918,#1206,.T.);
#2302=EDGE_CURVE('',#1918,#1916,#1207,.T.);
#2303=EDGE_CURVE('',#1917,#1907,#1208,.T.);
#2304=EDGE_CURVE('',#1910,#1918,#1209,.T.);
#2305=EDGE_CURVE('',#1919,#1919,#1669,.T.);
#2306=EDGE_CURVE('',#1920,#1920,#1670,.T.);
#2307=EDGE_CURVE('',#1921,#1921,#1671,.T.);
#2308=EDGE_CURVE('',#1921,#1920,#1210,.T.);
#2309=EDGE_CURVE('',#1922,#1922,#1672,.T.);
#2310=EDGE_CURVE('',#1922,#1921,#1211,.T.);
#2311=EDGE_CURVE('',#1923,#1923,#1673,.T.);
#2312=EDGE_CURVE('',#1923,#1922,#1212,.T.);
#2313=EDGE_CURVE('',#1924,#1924,#1674,.T.);
#2314=EDGE_CURVE('',#1925,#1925,#1675,.F.);
#2315=EDGE_CURVE('',#1925,#1924,#1213,.T.);
#2316=EDGE_CURVE('',#1919,#1925,#1214,.T.);
#2999=ORIENTED_EDGE('',*,*,#2287,.T.);
#3000=ORIENTED_EDGE('',*,*,#2288,.T.);
#3001=ORIENTED_EDGE('',*,*,#2289,.T.);
#3002=ORIENTED_EDGE('',*,*,#2290,.F.);
#3003=ORIENTED_EDGE('',*,*,#2291,.T.);
#3004=ORIENTED_EDGE('',*,*,#2292,.T.);
#3005=ORIENTED_EDGE('',*,*,#2293,.T.);
#3006=ORIENTED_EDGE('',*,*,#2288,.F.);
#3007=ORIENTED_EDGE('',*,*,#2294,.T.);
#3008=ORIENTED_EDGE('',*,*,#2295,.T.);
#3009=ORIENTED_EDGE('',*,*,#2296,.T.);
#3010=ORIENTED_EDGE('',*,*,#2292,.F.);
#3011=ORIENTED_EDGE('',*,*,#2297,.T.);
#3012=ORIENTED_EDGE('',*,*,#2298,.T.);
#3013=ORIENTED_EDGE('',*,*,#2299,.T.);
#3014=ORIENTED_EDGE('',*,*,#2295,.F.);
#3015=ORIENTED_EDGE('',*,*,#2300,.T.);
#3016=ORIENTED_EDGE('',*,*,#2301,.T.);
#3017=ORIENTED_EDGE('',*,*,#2302,.T.);
#3018=ORIENTED_EDGE('',*,*,#2298,.F.);
#3019=ORIENTED_EDGE('',*,*,#2303,.T.);
#3020=ORIENTED_EDGE('',*,*,#2290,.T.);
#3021=ORIENTED_EDGE('',*,*,#2304,.T.);
#3022=ORIENTED_EDGE('',*,*,#2301,.F.);
#3023=ORIENTED_EDGE('',*,*,#2303,.F.);
#3024=ORIENTED_EDGE('',*,*,#2300,.F.);
#3025=ORIENTED_EDGE('',*,*,#2297,.F.);
#3026=ORIENTED_EDGE('',*,*,#2294,.F.);
#3027=ORIENTED_EDGE('',*,*,#2291,.F.);
#3028=ORIENTED_EDGE('',*,*,#2287,.F.);
#3029=ORIENTED_EDGE('',*,*,#2304,.F.);
#3030=ORIENTED_EDGE('',*,*,#2289,.F.);
#3031=ORIENTED_EDGE('',*,*,#2293,.F.);
#3032=ORIENTED_EDGE('',*,*,#2296,.F.);
#3033=ORIENTED_EDGE('',*,*,#2299,.F.);
#3034=ORIENTED_EDGE('',*,*,#2302,.F.);
#3035=ORIENTED_EDGE('',*,*,#2305,.F.);
#3036=ORIENTED_EDGE('',*,*,#2306,.F.);
#3037=ORIENTED_EDGE('',*,*,#2307,.F.);
#3038=ORIENTED_EDGE('',*,*,#2308,.T.);
#3039=ORIENTED_EDGE('',*,*,#2306,.T.);
#3040=ORIENTED_EDGE('',*,*,#2308,.F.);
#3041=ORIENTED_EDGE('',*,*,#2309,.F.);
#3042=ORIENTED_EDGE('',*,*,#2310,.T.);
#3043=ORIENTED_EDGE('',*,*,#2307,.T.);
#3044=ORIENTED_EDGE('',*,*,#2310,.F.);
#3045=ORIENTED_EDGE('',*,*,#2311,.F.);
#3046=ORIENTED_EDGE('',*,*,#2312,.T.);
#3047=ORIENTED_EDGE('',*,*,#2309,.T.);
#3048=ORIENTED_EDGE('',*,*,#2312,.F.);
#3049=ORIENTED_EDGE('',*,*,#2311,.T.);
#3050=ORIENTED_EDGE('',*,*,#2313,.F.);
#3051=ORIENTED_EDGE('',*,*,#2314,.F.);
#3052=ORIENTED_EDGE('',*,*,#2315,.T.);
#3053=ORIENTED_EDGE('',*,*,#2313,.T.);
#3054=ORIENTED_EDGE('',*,*,#2315,.F.);
#3055=ORIENTED_EDGE('',*,*,#2305,.T.);
#3056=ORIENTED_EDGE('',*,*,#2316,.T.);
#3057=ORIENTED_EDGE('',*,*,#2314,.T.);
#3058=ORIENTED_EDGE('',*,*,#2316,.F.);
#3352=CYLINDRICAL_SURFACE('',#4170,0.35);
#3353=CYLINDRICAL_SURFACE('',#4178,0.1954);
#3515=ADVANCED_FACE('',(#640),#453,.F.);
#3516=ADVANCED_FACE('',(#641),#454,.F.);
#3517=ADVANCED_FACE('',(#642),#455,.F.);
#3518=ADVANCED_FACE('',(#643),#456,.F.);
#3519=ADVANCED_FACE('',(#644),#457,.F.);
#3520=ADVANCED_FACE('',(#645),#458,.F.);
#3521=ADVANCED_FACE('',(#646),#459,.F.);
#3522=ADVANCED_FACE('',(#647),#460,.F.);
#3523=ADVANCED_FACE('',(#648),#461,.F.);
#3524=ADVANCED_FACE('',(#649),#462,.T.);
#3525=ADVANCED_FACE('',(#650),#166,.T.);
#3526=ADVANCED_FACE('',(#651),#3352,.T.);
#3527=ADVANCED_FACE('',(#652),#167,.T.);
#3528=ADVANCED_FACE('',(#653,#344),#463,.T.);
#3529=ADVANCED_FACE('',(#654),#168,.T.);
#3530=ADVANCED_FACE('',(#655),#3353,.T.);
#3607=CLOSED_SHELL('',(#3515,#3516,#3517,#3518,#3519,#3520,#3521,#3522));
#3608=CLOSED_SHELL('',(#3523,#3524,#3525,#3526,#3527,#3528,#3529,#3530));
#4155=AXIS2_PLACEMENT_3D('',#6209,#5039,#5040);
#4156=AXIS2_PLACEMENT_3D('',#6210,#5041,#5042);
#4157=AXIS2_PLACEMENT_3D('',#6219,#5047,#5048);
#4158=AXIS2_PLACEMENT_3D('',#6225,#5052,#5053);
#4159=AXIS2_PLACEMENT_3D('',#6231,#5057,#5058);
#4160=AXIS2_PLACEMENT_3D('',#6237,#5062,#5063);
#4161=AXIS2_PLACEMENT_3D('',#6243,#5067,#5068);
#4162=AXIS2_PLACEMENT_3D('',#6246,#5071,#5072);
#4163=AXIS2_PLACEMENT_3D('',#6247,#5073,#5074);
#4164=AXIS2_PLACEMENT_3D('',#6248,#5075,#5076);
#4165=AXIS2_PLACEMENT_3D('',#6250,#5077,#5078);
#4166=AXIS2_PLACEMENT_3D('',#6251,#5079,#5080);
#4167=AXIS2_PLACEMENT_3D('',#6253,#5081,#5082);
#4168=AXIS2_PLACEMENT_3D('',#6254,#5083,#5084);
#4169=AXIS2_PLACEMENT_3D('',#6256,#5085,#5086);
#4170=AXIS2_PLACEMENT_3D('',#6258,#5088,#5089);
#4171=AXIS2_PLACEMENT_3D('',#6260,#5090,#5091);
#4172=AXIS2_PLACEMENT_3D('',#6262,#5093,#5094);
#4173=AXIS2_PLACEMENT_3D('',#6264,#5095,#5096);
#4174=AXIS2_PLACEMENT_3D('',#6266,#5098,#5099);
#4175=AXIS2_PLACEMENT_3D('',#6268,#5100,#5101);
#4176=AXIS2_PLACEMENT_3D('',#6269,#5102,#5103);
#4177=AXIS2_PLACEMENT_3D('',#6271,#5104,#5105);
#4178=AXIS2_PLACEMENT_3D('',#6273,#5107,#5108);
#5039=DIRECTION('axis',(0.,0.,1.));
#5040=DIRECTION('refdir',(1.,0.,0.));
#5041=DIRECTION('center_axis',(0.866025403784439,0.,-0.5));
#5042=DIRECTION('ref_axis',(0.5,0.,0.866025403784439));
#5043=DIRECTION('',(-0.5,0.,-0.866025403784439));
#5044=DIRECTION('',(0.,-1.,0.));
#5045=DIRECTION('',(0.5,0.,0.866025403784439));
#5046=DIRECTION('',(0.,-1.,0.));
#5047=DIRECTION('center_axis',(1.60246890531964E-16,0.,-1.));
#5048=DIRECTION('ref_axis',(1.,0.,1.60246890531964E-16));
#5049=DIRECTION('',(-1.,0.,-1.60246890531964E-16));
#5050=DIRECTION('',(0.,-1.,0.));
#5051=DIRECTION('',(1.,0.,1.60246890531964E-16));
#5052=DIRECTION('center_axis',(-0.866025403784439,0.,-0.5));
#5053=DIRECTION('ref_axis',(0.5,0.,-0.866025403784439));
#5054=DIRECTION('',(-0.5,0.,0.866025403784439));
#5055=DIRECTION('',(0.,-1.,0.));
#5056=DIRECTION('',(0.5,0.,-0.866025403784439));
#5057=DIRECTION('center_axis',(-0.866025403784439,0.,0.5));
#5058=DIRECTION('ref_axis',(-0.5,0.,-0.866025403784439));
#5059=DIRECTION('',(0.5,0.,0.866025403784439));
#5060=DIRECTION('',(0.,-1.,0.));
#5061=DIRECTION('',(-0.5,0.,-0.866025403784439));
#5062=DIRECTION('center_axis',(-1.60246890531964E-16,0.,1.));
#5063=DIRECTION('ref_axis',(-1.,0.,-1.60246890531964E-16));
#5064=DIRECTION('',(1.,0.,1.60246890531964E-16));
#5065=DIRECTION('',(0.,-1.,0.));
#5066=DIRECTION('',(-1.,0.,-1.60246890531964E-16));
#5067=DIRECTION('center_axis',(0.866025403784439,0.,0.5));
#5068=DIRECTION('ref_axis',(-0.5,0.,0.866025403784439));
#5069=DIRECTION('',(0.5,0.,-0.866025403784439));
#5070=DIRECTION('',(-0.5,0.,0.866025403784439));
#5071=DIRECTION('center_axis',(0.,1.,0.));
#5072=DIRECTION('ref_axis',(1.,0.,0.));
#5073=DIRECTION('center_axis',(0.,-1.,0.));
#5074=DIRECTION('ref_axis',(0.,0.,-1.));
#5075=DIRECTION('center_axis',(0.,1.,0.));
#5076=DIRECTION('ref_axis',(1.,0.,0.));
#5077=DIRECTION('center_axis',(0.,1.,0.));
#5078=DIRECTION('ref_axis',(1.,0.,0.));
#5079=DIRECTION('center_axis',(0.,1.,0.));
#5080=DIRECTION('ref_axis',(0.,0.,1.));
#5081=DIRECTION('center_axis',(0.,-1.,0.));
#5082=DIRECTION('ref_axis',(1.,0.,0.));
#5083=DIRECTION('center_axis',(0.,-1.,0.));
#5084=DIRECTION('ref_axis',(1.,0.,0.));
#5085=DIRECTION('center_axis',(0.,-1.,0.));
#5086=DIRECTION('ref_axis',(1.,0.,0.));
#5087=DIRECTION('',(0.707106781186547,0.707106781186548,8.65956056235493E-17));
#5088=DIRECTION('center_axis',(0.,-1.,0.));
#5089=DIRECTION('ref_axis',(1.,0.,0.));
#5090=DIRECTION('center_axis',(0.,-1.,0.));
#5091=DIRECTION('ref_axis',(1.,0.,0.));
#5092=DIRECTION('',(0.,1.,0.));
#5093=DIRECTION('center_axis',(0.,1.,0.));
#5094=DIRECTION('ref_axis',(1.,0.,0.));
#5095=DIRECTION('center_axis',(0.,-1.,0.));
#5096=DIRECTION('ref_axis',(1.,0.,0.));
#5097=DIRECTION('',(-0.707106781186547,0.707106781186548,-8.65956056235493E-17));
#5098=DIRECTION('center_axis',(0.,-1.,0.));
#5099=DIRECTION('ref_axis',(0.,0.,-1.));
#5100=DIRECTION('center_axis',(0.,-1.,0.));
#5101=DIRECTION('ref_axis',(1.,0.,0.));
#5102=DIRECTION('center_axis',(0.,1.,0.));
#5103=DIRECTION('ref_axis',(1.,0.,0.));
#5104=DIRECTION('center_axis',(0.,1.,0.));
#5105=DIRECTION('ref_axis',(1.,0.,0.));
#5106=DIRECTION('',(-0.447213595499958,0.894427190999916,-5.47678698264203E-17));
#5107=DIRECTION('center_axis',(0.,-1.,0.));
#5108=DIRECTION('ref_axis',(1.,0.,0.));
#5109=DIRECTION('',(0.,1.,0.));
#6209=CARTESIAN_POINT('',(0.,0.,0.));
#6210=CARTESIAN_POINT('Origin',(0.0866025403784439,-0.4,-0.15));
#6211=CARTESIAN_POINT('',(0.173205080756888,-0.4,0.));
#6212=CARTESIAN_POINT('',(0.0866025403784439,-0.4,-0.15));
#6213=CARTESIAN_POINT('',(0.173205080756888,-0.4,0.));
#6214=CARTESIAN_POINT('',(0.0866025403784439,-0.64,-0.15));
#6215=CARTESIAN_POINT('',(0.0866025403784439,-0.4,-0.15));
#6216=CARTESIAN_POINT('',(0.173205080756888,-0.64,0.));
#6217=CARTESIAN_POINT('',(0.173205080756888,-0.64,0.));
#6218=CARTESIAN_POINT('',(0.173205080756888,-0.4,0.));
#6219=CARTESIAN_POINT('Origin',(-0.0866025403784438,-0.4,-0.15));
#6220=CARTESIAN_POINT('',(-0.0866025403784438,-0.4,-0.15));
#6221=CARTESIAN_POINT('',(0.0866025403784439,-0.4,-0.15));
#6222=CARTESIAN_POINT('',(-0.0866025403784438,-0.64,-0.15));
#6223=CARTESIAN_POINT('',(-0.0866025403784438,-0.4,-0.15));
#6224=CARTESIAN_POINT('',(0.0866025403784439,-0.64,-0.15));
#6225=CARTESIAN_POINT('Origin',(-0.173205080756888,-0.4,-2.77555756156289E-17));
#6226=CARTESIAN_POINT('',(-0.173205080756888,-0.4,-2.12115047744981E-17));
#6227=CARTESIAN_POINT('',(-0.0866025403784438,-0.4,-0.15));
#6228=CARTESIAN_POINT('',(-0.173205080756888,-0.64,-2.77555756156289E-17));
#6229=CARTESIAN_POINT('',(-0.173205080756888,-0.4,-2.12115047744981E-17));
#6230=CARTESIAN_POINT('',(-0.0866025403784438,-0.64,-0.15));
#6231=CARTESIAN_POINT('Origin',(-0.0866025403784439,-0.4,0.15));
#6232=CARTESIAN_POINT('',(-0.0866025403784439,-0.4,0.15));
#6233=CARTESIAN_POINT('',(-0.173205080756888,-0.4,-2.12115047744981E-17));
#6234=CARTESIAN_POINT('',(-0.0866025403784439,-0.64,0.15));
#6235=CARTESIAN_POINT('',(-0.0866025403784439,-0.4,0.15));
#6236=CARTESIAN_POINT('',(-0.173205080756888,-0.64,-2.12115047744981E-17));
#6237=CARTESIAN_POINT('Origin',(0.0866025403784439,-0.4,0.15));
#6238=CARTESIAN_POINT('',(0.0866025403784439,-0.4,0.15));
#6239=CARTESIAN_POINT('',(-0.0866025403784439,-0.4,0.15));
#6240=CARTESIAN_POINT('',(0.0866025403784439,-0.64,0.15));
#6241=CARTESIAN_POINT('',(0.0866025403784439,-0.4,0.15));
#6242=CARTESIAN_POINT('',(-0.0866025403784439,-0.64,0.15));
#6243=CARTESIAN_POINT('Origin',(0.173205080756888,-0.4,0.));
#6244=CARTESIAN_POINT('',(0.0866025403784439,-0.4,0.15));
#6245=CARTESIAN_POINT('',(0.0866025403784439,-0.64,0.15));
#6246=CARTESIAN_POINT('Origin',(0.,-0.4,-2.77555756156289E-17));
#6247=CARTESIAN_POINT('Origin',(0.,-0.64,-2.77555756156289E-17));
#6248=CARTESIAN_POINT('Origin',(0.,-1.,0.));
#6249=CARTESIAN_POINT('',(-0.1954,-1.,2.39295984553393E-17));
#6250=CARTESIAN_POINT('Origin',(0.,-1.,0.));
#6251=CARTESIAN_POINT('Origin',(0.3,0.4,0.));
#6252=CARTESIAN_POINT('',(-0.3,0.4,-3.67394039744206E-17));
#6253=CARTESIAN_POINT('Origin',(0.,0.4,0.));
#6254=CARTESIAN_POINT('Origin',(0.,0.375,0.));
#6255=CARTESIAN_POINT('',(-0.35,0.35,-4.28626379701573E-17));
#6256=CARTESIAN_POINT('Origin',(0.,0.35,0.));
#6257=CARTESIAN_POINT('',(-0.325,0.375,-3.9801020972289E-17));
#6258=CARTESIAN_POINT('Origin',(0.,0.19,0.));
#6259=CARTESIAN_POINT('',(-0.35,0.03,-4.28626379701574E-17));
#6260=CARTESIAN_POINT('Origin',(0.,0.03,0.));
#6261=CARTESIAN_POINT('',(-0.35,0.19,-4.28626379701574E-17));
#6262=CARTESIAN_POINT('Origin',(0.,0.0149999999999999,0.));
#6263=CARTESIAN_POINT('',(-0.32,-3.29597460435593E-17,-3.91886975727153E-17));
#6264=CARTESIAN_POINT('Origin',(0.,0.,0.));
#6265=CARTESIAN_POINT('',(-0.335,0.0149999999999999,-4.10256677714363E-17));
#6266=CARTESIAN_POINT('Origin',(0.22,0.,0.));
#6267=CARTESIAN_POINT('',(-0.22,-6.93889390390723E-18,-2.69422295812418E-17));
#6268=CARTESIAN_POINT('Origin',(0.,0.,0.));
#6269=CARTESIAN_POINT('Origin',(0.,-0.02,0.));
#6270=CARTESIAN_POINT('',(-0.1954,-0.0492,2.39295984553393E-17));
#6271=CARTESIAN_POINT('Origin',(0.,-0.0492,0.));
#6272=CARTESIAN_POINT('',(-0.21,-0.02,-2.57175827820944E-17));
#6273=CARTESIAN_POINT('Origin',(0.,-0.8,0.));
#6274=CARTESIAN_POINT('',(-0.1954,-0.8,-2.39295984553393E-17));
#6599=UNCERTAINTY_MEASURE_WITH_UNIT(LENGTH_MEASURE(0.001),#6639,
'DISTANCE_ACCURACY_VALUE',
'Maximum model space distance between geometric entities at asserted c
onnectivities');
#6609=UNCERTAINTY_MEASURE_WITH_UNIT(LENGTH_MEASURE(0.001),#6639,
'DISTANCE_ACCURACY_VALUE',
'Maximum model space distance between geometric entities at asserted c
onnectivities');
#6628=(
GEOMETRIC_REPRESENTATION_CONTEXT(3)
GLOBAL_UNCERTAINTY_ASSIGNED_CONTEXT((#6599))
GLOBAL_UNIT_ASSIGNED_CONTEXT((#6639,#6641,#6642))
REPRESENTATION_CONTEXT('','3D')
);
#6638=(
GEOMETRIC_REPRESENTATION_CONTEXT(3)
GLOBAL_UNCERTAINTY_ASSIGNED_CONTEXT((#6609))
GLOBAL_UNIT_ASSIGNED_CONTEXT((#6639,#6641,#6642))
REPRESENTATION_CONTEXT('','3D')
);
#6639=(
LENGTH_UNIT()
NAMED_UNIT(*)
SI_UNIT(.CENTI.,.METRE.)
);
#6641=(
NAMED_UNIT(*)
PLANE_ANGLE_UNIT()
SI_UNIT($,.RADIAN.)
);
#6642=(
NAMED_UNIT(*)
SI_UNIT($,.STERADIAN.)
SOLID_ANGLE_UNIT()
);
#6661=SHAPE_DEFINITION_REPRESENTATION(#6689,#6755);
#6689=PRODUCT_DEFINITION_SHAPE('',$,#6784);
#6755=SHAPE_REPRESENTATION('',(#4155),#6628);
#6765=PRODUCT_DEFINITION_CONTEXT('part definition',#6851,'design');
#6784=PRODUCT_DEFINITION('M4x10 Cap Screw','M4x10 Cap Screw',#6812,#6765);
#6812=PRODUCT_DEFINITION_FORMATION('',$,#6871);
#6851=APPLICATION_CONTEXT(
'Core Data for Automotive Mechanical Design Process');
#6852=PRODUCT_CONTEXT('part definition',#6851,'mechanical');
#6871=PRODUCT('M4x10 Cap Screw','M4x10 Cap Screw','M4x10 Cap Screw',(#6852));
#6944=COLOUR_RGB('Black',0.12,0.14,0.17);
#6945=FILL_AREA_STYLE_COLOUR('',#6944);
#6946=FILL_AREA_STYLE('',(#6945));
#6947=SURFACE_STYLE_FILL_AREA(#6946);
#6948=SURFACE_SIDE_STYLE('',(#6947));
#6949=SURFACE_STYLE_USAGE(.BOTH.,#6948);
#6950=PRESENTATION_STYLE_ASSIGNMENT((#6949));
ENDSEC;
END-ISO-10303-21;
